ISO-10303-21;
HEADER;
FILE_DESCRIPTION (('STEP AP214'),
    '1' );
FILE_NAME ('Square Thread Nut.step',
    '2026-10-09T10:51:02',
    ( '' ),
    ( '' ),
    'SwSTEP 2.0',
    'SolidWorks 2026',
    '' );
FILE_SCHEMA (( 'AUTOMOTIVE_DESIGN' ));
ENDSEC;

DATA;
#5=EDGE_LOOP ( 'NONE', ( #8309, #15407, #11959, #15911 ) ) ;
#45=DIRECTION ( 'NONE',  ( -0.7161863329816251511, -0.003898296230782347539, -0.6978982302147140881 ) ) ;
#110=EDGE_CURVE ( 'NONE', #3828, #14649, #15744, .T. ) ;
#167=VECTOR ( 'NONE', #3527, 999.9999999999998863 ) ;
#173=CARTESIAN_POINT ( 'NONE',  ( -14.82979117956944037, 177.4987173824078468, 90.64024647396865930 ) ) ;
#183=DIRECTION ( 'NONE',  ( 7.125109674160325297E-05, -0.9999848031710252272, 0.005512562950849327591 ) ) ;
#186=DIRECTION ( 'NONE',  ( -0.01292394549866750231, -0.005513023399722823126, -0.9999012842304692006 ) ) ;
#195=DIRECTION ( 'NONE',  ( -0.9999164797902015955, -8.506845633049209592E-18, 0.01292414190464159611 ) ) ;
#294=DIRECTION ( 'NONE',  ( 0.7069973413461587697, 0.7070960354057281849, -0.01303671902605322945 ) ) ;
#324=ORIENTED_EDGE ( 'NONE', *, *, #12603, .F. ) ;
#333=DIRECTION ( 'NONE',  ( -0.7070981056135049458, 0.7070960354057279629, 0.005240777737525892203 ) ) ;
#337=ORIENTED_EDGE ( 'NONE', *, *, #2949, .T. ) ;
#365=MECHANICAL_DESIGN_GEOMETRIC_PRESENTATION_REPRESENTATION('',(#14686),#5105);
#422=PLANE ( 'NONE',  #12245 ) ;
#457=AXIS2_PLACEMENT_3D ( 'NONE', #9188, #1976, #17951 ) ;
#522=FACE_OUTER_BOUND ( 'NONE', #20407, .T. ) ;
#631=( NAMED_UNIT ( * ) PLANE_ANGLE_UNIT ( ) SI_UNIT ( $, .RADIAN. ) );
#638=VERTEX_POINT ( 'NONE', #15306 ) ;
#745=DIRECTION ( 'NONE',  ( 7.125109674160325297E-05, -0.9999848031710252272, 0.005512562950849327591 ) ) ;
#856=CARTESIAN_POINT ( 'NONE',  ( 19.46746992363642903, 137.6261247937603969, 113.4190577045456223 ) ) ;
#897=CARTESIAN_POINT ( 'NONE',  ( -16.53237339268049055, 177.6255169206013989, 113.6638242950787543 ) ) ;
#898=AXIS2_PLACEMENT_3D ( 'NONE', #8279, #13568, #18612 ) ;
#907=FACE_OUTER_BOUND ( 'NONE', #9310, .T. ) ;
#915=LINE ( 'NONE', #13745, #2471 ) ;
#965=ORIENTED_EDGE ( 'NONE', *, *, #3429, .F. ) ;
#986=EDGE_CURVE ( 'NONE', #10785, #11013, #915, .T. ) ;
#987=ORIENTED_EDGE ( 'NONE', *, *, #15352, .T. ) ;
#991=DIRECTION ( 'NONE',  ( -0.6979091139780407849, 0.003898296230782323252, 0.7161757269782906832 ) ) ;
#1009=ORIENTED_EDGE ( 'NONE', *, *, #8835, .T. ) ;
#1082=DIRECTION ( 'NONE',  ( -7.125109674160325297E-05, 0.9999848031710253382, -0.005512562950849328458 ) ) ;
#1170=DIRECTION ( 'NONE',  ( 0.7070981056135045018, -0.7070960354057282959, -0.005240777737525213927 ) ) ;
#1186=LINE ( 'NONE', #18732, #11455 ) ;
#1202=AXIS2_PLACEMENT_3D ( 'NONE', #15669, #3891, #6909 ) ;
#1233=ORIENTED_EDGE ( 'NONE', *, *, #7992, .F. ) ;
#1262=VECTOR ( 'NONE', #12221, 999.9999999999998863 ) ;
#1275=AXIS2_PLACEMENT_3D ( 'NONE', #8915, #6967, #5234 ) ;
#1278=EDGE_CURVE ( 'NONE', #7668, #3399, #21703, .T. ) ;
#1295=FACE_OUTER_BOUND ( 'NONE', #10911, .T. ) ;
#1310=ORIENTED_EDGE ( 'NONE', *, *, #20423, .T. ) ;
#1369=ORIENTED_EDGE ( 'NONE', *, *, #4719, .F. ) ;
#1379=LINE ( 'NONE', #8465, #21418 ) ;
#1395=DIRECTION ( 'NONE',  ( 1.000000000000000000, 0.000000000000000000, 0.000000000000000000 ) ) ;
#1412=ORIENTED_EDGE ( 'NONE', *, *, #22523, .T. ) ;
#1470=ORIENTED_EDGE ( 'NONE', *, *, #22245, .T. ) ;
#1477=CARTESIAN_POINT ( 'NONE',  ( 9.466310095025644245, 165.6256992825491068, 113.3939473609682551 ) ) ;
#1485=DIRECTION ( 'NONE',  ( -0.6979091139780387865, 0.003898296230782432540, 0.7161757269782926816 ) ) ;
#1508=CARTESIAN_POINT ( 'NONE',  ( 19.46461987976676511, 177.6255169206013989, 113.1985551865116406 ) ) ;
#1564=CIRCLE ( 'NONE', #16995, 8.000000000000000000 ) ;
#1574=DIRECTION ( 'NONE',  ( -7.125109674160325297E-05, 0.9999848031710253382, -0.005512562950849327591 ) ) ;
#1583=DIRECTION ( 'NONE',  ( 7.125109674160325297E-05, -0.9999848031710253382, 0.005512562950849327591 ) ) ;
#1596=ORIENTED_EDGE ( 'NONE', *, *, #4557, .T. ) ;
#1702=CARTESIAN_POINT ( 'NONE',  ( 9.143198533613464463, 165.4878681845327151, 88.39541535392230287 ) ) ;
#1706=CARTESIAN_POINT ( 'NONE',  ( 17.30323760145302714, 177.5566041281049081, 100.7256374174400548 ) ) ;
#1860=LINE ( 'NONE', #8855, #9890 ) ;
#1885=DIRECTION ( 'NONE',  ( 0.01292394549866728373, 0.005513023399720296501, 0.9999012842304693116 ) ) ;
#1908=ORIENTED_EDGE ( 'NONE', *, *, #12235, .T. ) ;
#1916=APPLICATION_CONTEXT ( 'automotive_design' ) ;
#1918=DIRECTION ( 'NONE',  ( 7.125109674160325297E-05, -0.9999848031710253382, 0.005512562950849327591 ) ) ;
#1919=ORIENTED_EDGE ( 'NONE', *, *, #14078, .T. ) ;
#1947=CLOSED_SHELL ( 'NONE', ( #12781, #6146, #12871, #3592, #4295, #12353, #17971, #17861, #11488, #11202, #3726, #7553, #6285, #13146, #19336, #8004, #12457, #13217, #3035, #16807, #11624, #2048, #17096, #16134, #7945, #20890, #15996, #16001 ) ) ;
#1976=DIRECTION ( 'NONE',  ( 0.01292394549866728200, 0.005513023399720295634, 0.9999012842304692006 ) ) ;
#2007=DIRECTION ( 'NONE',  ( 0.6979091139780386754, -0.003898296230784643879, -0.7161757269782926816 ) ) ;
#2046=CARTESIAN_POINT ( 'NONE',  ( -16.82962413914983912, 177.4987173824078468, 90.66609475777795524 ) ) ;
#2048=ADVANCED_FACE ( 'NONE', ( #19222 ), #3710, .T. ) ;
#2054=ORIENTED_EDGE ( 'NONE', *, *, #3429, .T. ) ;
#2126=EDGE_CURVE ( 'NONE', #5284, #19030, #14428, .T. ) ;
#2143=AXIS2_PLACEMENT_3D ( 'NONE', #20458, #20572, #8295 ) ;
#2229=EDGE_CURVE ( 'NONE', #10627, #15063, #6736, .T. ) ;
#2234=DIRECTION ( 'NONE',  ( 7.125109674160325297E-05, -0.9999848031710252272, 0.005512562950849327591 ) ) ;
#2277=ORIENTED_EDGE ( 'NONE', *, *, #4000, .F. ) ;
#2288=ORIENTED_EDGE ( 'NONE', *, *, #7682, .F. ) ;
#2343=CIRCLE ( 'NONE', #12636, 8.000000000000000000 ) ;
#2352=VECTOR ( 'NONE', #6466, 1000.000000000000227 ) ;
#2429=CARTESIAN_POINT ( 'NONE',  ( -14.85549656837329557, 175.4877217292663545, 88.65146903140943380 ) ) ;
#2431=CARTESIAN_POINT ( 'NONE',  ( 13.80495188559012121, 157.5998335170374389, 100.8808865402689463 ) ) ;
#2471=VECTOR ( 'NONE', #16768, 1000.000000000000227 ) ;
#2538=DIRECTION ( 'NONE',  ( 0.7070981056135046128, -0.7070960354057282959, -0.005240777737524086356 ) ) ;
#2549=VECTOR ( 'NONE', #21134, 1000.000000000000000 ) ;
#2557=DIRECTION ( 'NONE',  ( 0.01292394549866728373, 0.005513023399720296501, 0.9999012842304693116 ) ) ;
#2687=AXIS2_PLACEMENT_3D ( 'NONE', #17748, #8864, #17617 ) ;
#2710=AXIS2_PLACEMENT_3D ( 'NONE', #4278, #4171, #18212 ) ;
#2725=DIRECTION ( 'NONE',  ( 0.9999164797902017066, 9.297033629063200522E-18, -0.01292414190464145386 ) ) ;
#2733=VECTOR ( 'NONE', #17796, 1000.000000000000114 ) ;
#2770=PRODUCT_DEFINITION_SHAPE ( 'NONE', 'NONE',  #9157 ) ;
#2785=CARTESIAN_POINT ( 'NONE',  ( 13.84903886101111681, 155.5756827379013885, 104.2918126654085995 ) ) ;
#2804=DIRECTION ( 'NONE',  ( 7.125109674160325297E-05, -0.9999848031710253382, 0.005512562950849327591 ) ) ;
#2823=( NAMED_UNIT ( * ) SI_UNIT ( $, .STERADIAN. ) SOLID_ANGLE_UNIT ( ) );
#2949=EDGE_CURVE ( 'NONE', #11929, #20403, #4367, .T. ) ;
#2960=EDGE_LOOP ( 'NONE', ( #2054, #5081, #15427, #19986 ) ) ;
#2970=AXIS2_PLACEMENT_3D ( 'NONE', #16523, #4083, #11117 ) ;
#2997=DIRECTION ( 'NONE',  ( 0.9999164797902015955, 8.506845633049208051E-18, -0.01292414190464159611 ) ) ;
#3035=ADVANCED_FACE ( 'NONE', ( #3639 ), #6855, .T. ) ;
#3057=CARTESIAN_POINT ( 'NONE',  ( -11.14887313374392264, 155.5756827379013885, 104.6149162130246140 ) ) ;
#3068=CARTESIAN_POINT ( 'NONE',  ( -6.532353581617583060, 165.6256992825491068, 113.6007336314425231 ) ) ;
#3086=EDGE_CURVE ( 'NONE', #16183, #20403, #17837, .T. ) ;
#3102=CARTESIAN_POINT ( 'NONE',  ( 0.000000000000000000, 0.000000000000000000, 0.000000000000000000 ) ) ;
#3279=VECTOR ( 'NONE', #12398, 1000.000000000000227 ) ;
#3313=ORIENTED_EDGE ( 'NONE', *, *, #3503, .T. ) ;
#3373=LINE ( 'NONE', #10159, #10433 ) ;
#3399=VERTEX_POINT ( 'NONE', #17691 ) ;
#3429=EDGE_CURVE ( 'NONE', #21699, #10079, #3534, .T. ) ;
#3433=AXIS2_PLACEMENT_3D ( 'NONE', #9583, #745, #13153 ) ;
#3445=EDGE_LOOP ( 'NONE', ( #21361, #7679, #1908, #5336 ) ) ;
#3503=EDGE_CURVE ( 'NONE', #14111, #22024, #10997, .T. ) ;
#3514=DIRECTION ( 'NONE',  ( 7.125109674160325297E-05, -0.9999848031710253382, 0.005512562950849327591 ) ) ;
#3527=DIRECTION ( 'NONE',  ( 0.01292394549866728373, 0.005513023399720296501, 0.9999012842304693116 ) ) ;
#3534=LINE ( 'NONE', #10546, #3279 ) ;
#3582=EDGE_LOOP ( 'NONE', ( #4918, #19219 ) ) ;
#3592=ADVANCED_FACE ( 'NONE', ( #907 ), #11686, .F. ) ;
#3620=EDGE_CURVE ( 'NONE', #10079, #10627, #21493, .T. ) ;
#3623=CARTESIAN_POINT ( 'NONE',  ( -14.53254043310009358, 177.6255169206013989, 113.6379760112694584 ) ) ;
#3635=CARTESIAN_POINT ( 'NONE',  ( -11.14759061400257423, 137.5759562808229362, 104.7141423461399086 ) ) ;
#3639=FACE_OUTER_BOUND ( 'NONE', #14179, .T. ) ;
#3642=LINE ( 'NONE', #5016, #12660 ) ;
#3679=CARTESIAN_POINT ( 'NONE',  ( 17.43893902918902938, 177.6144908738019694, 111.2246009018600006 ) ) ;
#3710=PLANE ( 'NONE',  #9474 ) ;
#3724=DIRECTION ( 'NONE',  ( 0.01292394549866728200, 0.005513023399720295634, 0.9999012842304692006 ) ) ;
#3726=ADVANCED_FACE ( 'NONE', ( #14530, #4489, #19763 ), #13039, .F. ) ;
#3746=ORIENTED_EDGE ( 'NONE', *, *, #21604, .T. ) ;
#3751=CARTESIAN_POINT ( 'NONE',  ( -16.82677409528017520, 137.4993252555668164, 90.88659727581192271 ) ) ;
#3828=VERTEX_POINT ( 'NONE', #2785 ) ;
#3836=CARTESIAN_POINT ( 'NONE',  ( 17.14183078491316436, 175.4877217292663545, 88.23789649046089778 ) ) ;
#3863=CARTESIAN_POINT ( 'NONE',  ( -6.855465143029762842, 165.4878681845327151, 88.60220162439657088 ) ) ;
#3891=DIRECTION ( 'NONE',  ( -0.7070981056135072773, 0.7070960354057256314, 0.005240777737525932969 ) ) ;
#3925=ORIENTED_EDGE ( 'NONE', *, *, #14030, .F. ) ;
#3954=CARTESIAN_POINT ( 'NONE',  ( 13.76243855136152838, 137.5384677217048193, 97.59171006575670049 ) ) ;
#3988=ORIENTED_EDGE ( 'NONE', *, *, #5250, .F. ) ;
#3996=CARTESIAN_POINT ( 'NONE',  ( 17.14183078491316436, 175.4877217292663545, 88.23789649046089778 ) ) ;
#4000=EDGE_CURVE ( 'NONE', #16185, #5296, #21189, .T. ) ;
#4011=LINE ( 'NONE', #16357, #14018 ) ;
#4022=VECTOR ( 'NONE', #7656, 999.9999999999998863 ) ;
#4023=DIRECTION ( 'NONE',  ( 0.01292394549866738088, 0.005513023399720295634, 0.9999012842304693116 ) ) ;
#4033=DIRECTION ( 'NONE',  ( -7.125109674160325297E-05, 0.9999848031710253382, -0.005512562950849328458 ) ) ;
#4038=AXIS2_PLACEMENT_3D ( 'NONE', #9351, #13057, #2804 ) ;
#4083=DIRECTION ( 'NONE',  ( 7.125109674160325297E-05, -0.9999848031710252272, 0.005512562950849327591 ) ) ;
#4130=DIRECTION ( 'NONE',  ( 0.009088227368120106384, 0.7109943316365106014, 0.7031390079522377157 ) ) ;
#4147=ADVANCED_BREP_SHAPE_REPRESENTATION ( '', ( #17421, #6292 ), #12539 ) ;
#4156=ORIENTED_EDGE ( 'NONE', *, *, #11113, .F. ) ;
#4171=DIRECTION ( 'NONE',  ( 7.125109674160325297E-05, -0.9999848031710252272, 0.005512562950849327591 ) ) ;
#4182=CIRCLE ( 'NONE', #17051, 3.399999999999991918 ) ;
#4235=UNCERTAINTY_MEASURE_WITH_UNIT (LENGTH_MEASURE( 1.000000000000000082E-05 ), #18564, 'distance_accuracy_value', 'NONE');
#4275=EDGE_CURVE ( 'NONE', #10365, #20395, #20111, .T. ) ;
#4278=CARTESIAN_POINT ( 'NONE',  ( 13.80509744631564750, 155.5569384583423300, 100.8921482990249956 ) ) ;
#4283=EDGE_CURVE ( 'NONE', #7668, #10785, #9696, .T. ) ;
#4295=ADVANCED_FACE ( 'NONE', ( #18963 ), #15223, .F. ) ;
#4367=CIRCLE ( 'NONE', #17219, 3.399999999999991918 ) ;
#4368=LINE ( 'NONE', #6557, #2549 ) ;
#4375=DIRECTION ( 'NONE',  ( 0.9999164797902015955, 8.506845633049208051E-18, -0.01292414190464159611 ) ) ;
#4382=DIRECTION ( 'NONE',  ( -0.01104128644981280764, -0.5197558313507618655, -0.8542435049623797738 ) ) ;
#4386=ORIENTED_EDGE ( 'NONE', *, *, #8773, .F. ) ;
#4424=PLANE ( 'NONE',  #21723 ) ;
#4435=EDGE_CURVE ( 'NONE', #10785, #19030, #5765, .T. ) ;
#4461=VERTEX_POINT ( 'NONE', #173 ) ;
#4486=DIRECTION ( 'NONE',  ( 7.125109674160325297E-05, -0.9999848031710252272, 0.005512562950849327591 ) ) ;
#4489=FACE_BOUND ( 'NONE', #21574, .T. ) ;
#4497=LINE ( 'NONE', #9798, #2352 ) ;
#4535=EDGE_LOOP ( 'NONE', ( #4386, #11606, #21208 ) ) ;
#4548=VECTOR ( 'NONE', #1170, 1000.000000000000114 ) ;
#4557=EDGE_CURVE ( 'NONE', #5284, #10079, #19891, .T. ) ;
#4685=CARTESIAN_POINT ( 'NONE',  ( 19.43891449096291169, 175.6145212674599065, 111.2097777439524151 ) ) ;
#4719=EDGE_CURVE ( 'NONE', #3399, #10079, #4368, .T. ) ;
#4750=DIRECTION ( 'NONE',  ( -0.01292394549866750231, -0.005513023399722823126, -0.9999012842304692006 ) ) ;
#4759=CARTESIAN_POINT ( 'NONE',  ( -11.19281454843939194, 155.5569384583423300, 101.2152518466410243 ) ) ;
#4762=EDGE_LOOP ( 'NONE', ( #18542, #965, #20284, #14850 ) ) ;
#4770=VECTOR ( 'NONE', #20499, 1000.000000000000227 ) ;
#4848=CONICAL_SURFACE ( 'NONE', #15890, 3.399999999999991918, 1.029744258676652313 ) ;
#4918=ORIENTED_EDGE ( 'NONE', *, *, #20196, .F. ) ;
#4932=FACE_OUTER_BOUND ( 'NONE', #8930, .T. ) ;
#4955=DIRECTION ( 'NONE',  ( -0.9999164797902017066, -9.297033629063200522E-18, 0.01292414190464145386 ) ) ;
#4998=EDGE_CURVE ( 'NONE', #5939, #13046, #17792, .T. ) ;
#5016=CARTESIAN_POINT ( 'NONE',  ( -15.84248910266482646, 175.4932347526660692, 89.66429445754454264 ) ) ;
#5081=ORIENTED_EDGE ( 'NONE', *, *, #3620, .T. ) ;
#5096=CARTESIAN_POINT ( 'NONE',  ( -11.19153202869804353, 137.5572120012638777, 101.3144779797563189 ) ) ;
#5105=( GEOMETRIC_REPRESENTATION_CONTEXT ( 3 ) GLOBAL_UNCERTAINTY_ASSIGNED_CONTEXT ( ( #4235 ) ) GLOBAL_UNIT_ASSIGNED_CONTEXT ( ( #18564, #13513, #2823 ) ) REPRESENTATION_CONTEXT ( 'NONE', 'WORKASPACE' ) );
#5113=ORIENTED_EDGE ( 'NONE', *, *, #7992, .T. ) ;
#5114=CARTESIAN_POINT ( 'NONE',  ( -11.23547344339351284, 137.5384677217048193, 97.91481361337272915 ) ) ;
#5162=CIRCLE ( 'NONE', #18736, 3.399999999999991918 ) ;
#5234=DIRECTION ( 'NONE',  ( -0.01292394549866750231, -0.005513023399722823126, -0.9999012842304692006 ) ) ;
#5245=ORIENTED_EDGE ( 'NONE', *, *, #2229, .T. ) ;
#5250=EDGE_CURVE ( 'NONE', #14111, #4461, #1860, .T. ) ;
#5255=CARTESIAN_POINT ( 'NONE',  ( -16.82677409528017520, 137.4993252555668164, 90.88659727581192271 ) ) ;
#5284=VERTEX_POINT ( 'NONE', #12895 ) ;
#5296=VERTEX_POINT ( 'NONE', #7485 ) ;
#5336=ORIENTED_EDGE ( 'NONE', *, *, #6130, .T. ) ;
#5367=FACE_OUTER_BOUND ( 'NONE', #9373, .T. ) ;
#5391=LINE ( 'NONE', #5635, #22427 ) ;
#5418=ORIENTED_EDGE ( 'NONE', *, *, #6410, .T. ) ;
#5441=CARTESIAN_POINT ( 'NONE',  ( 17.46763696405603028, 137.6261247937603969, 113.4449059883549040 ) ) ;
#5443=CARTESIAN_POINT ( 'NONE',  ( -15.55823355279088638, 176.6145060706309380, 111.6566101476640114 ) ) ;
#5511=LINE ( 'NONE', #9065, #11825 ) ;
#5592=AXIS2_PLACEMENT_3D ( 'NONE', #19279, #14139, #333 ) ;
#5619=AXIS2_PLACEMENT_3D ( 'NONE', #15998, #19404, #17364 ) ;
#5635=CARTESIAN_POINT ( 'NONE',  ( -14.82979117956944037, 177.4987173824078468, 90.64024647396865930 ) ) ;
#5641=LINE ( 'NONE', #19751, #12888 ) ;
#5642=FACE_OUTER_BOUND ( 'NONE', #2960, .T. ) ;
#5660=CARTESIAN_POINT ( 'NONE',  ( 19.43891449096291169, 175.6145212674599065, 111.2097777439524151 ) ) ;
#5672=DIRECTION ( 'NONE',  ( 0.9999164797902015955, 8.772500386246550856E-18, -0.01292414190464154927 ) ) ;
#5719=PLANE ( 'NONE',  #1202 ) ;
#5734=EDGE_LOOP ( 'NONE', ( #1233, #16746, #12694, #19620 ) ) ;
#5747=DIRECTION ( 'NONE',  ( 0.9999164797902017066, 0.000000000000000000, -0.01292414190464177826 ) ) ;
#5765=LINE ( 'NONE', #5660, #17593 ) ;
#5775=( LENGTH_UNIT ( ) NAMED_UNIT ( * ) SI_UNIT ( .MILLI., .METRE. ) );
#5784=AXIS2_PLACEMENT_3D ( 'NONE', #16710, #4033, #2557 ) ;
#5878=AXIS2_PLACEMENT_3D ( 'NONE', #16161, #3724, #12706 ) ;
#5913=EDGE_CURVE ( 'NONE', #19030, #20077, #16073, .T. ) ;
#5939=VERTEX_POINT ( 'NONE', #8912 ) ;
#5990=CARTESIAN_POINT ( 'NONE',  ( 17.14168828271968437, 177.4876913356084174, 88.22687136455920154 ) ) ;
#6044=ORIENTED_EDGE ( 'NONE', *, *, #14479, .F. ) ;
#6130=EDGE_CURVE ( 'NONE', #6788, #13046, #17642, .T. ) ;
#6146=ADVANCED_FACE ( 'NONE', ( #10963 ), #10286, .F. ) ;
#6149=CARTESIAN_POINT ( 'NONE',  ( 19.46746992363642903, 137.6261247937603969, 113.4190577045456223 ) ) ;
#6151=DIRECTION ( 'NONE',  ( 7.125109674160325297E-05, -0.9999848031710253382, 0.005512562950849327591 ) ) ;
#6211=LINE ( 'NONE', #18514, #6640 ) ;
#6267=VECTOR ( 'NONE', #17063, 1000.000000000000227 ) ;
#6285=ADVANCED_FACE ( 'NONE', ( #522 ), #20122, .F. ) ;
#6292=AXIS2_PLACEMENT_3D ( 'NONE', #3102, #12069, #1395 ) ;
#6410=EDGE_CURVE ( 'NONE', #10365, #3828, #15238, .T. ) ;
#6452=ORIENTED_EDGE ( 'NONE', *, *, #4283, .T. ) ;
#6453=DIRECTION ( 'NONE',  ( 0.7161863329816247070, 0.003898296230784560612, 0.6978982302147144212 ) ) ;
#6459=ORIENTED_EDGE ( 'NONE', *, *, #110, .T. ) ;
#6466=DIRECTION ( 'NONE',  ( -0.9999164797902015955, -8.772500386246549315E-18, 0.01292414190464155101 ) ) ;
#6552=DIRECTION ( 'NONE',  ( -0.01292394549866742771, -0.005513023399720295634, -0.9999012842304693116 ) ) ;
#6557=CARTESIAN_POINT ( 'NONE',  ( 17.14183078491316436, 175.4877217292663545, 88.23789649046089778 ) ) ;
#6621=VECTOR ( 'NONE', #13172, 999.9999999999998863 ) ;
#6628=ORIENTED_EDGE ( 'NONE', *, *, #18497, .F. ) ;
#6640=VECTOR ( 'NONE', #6453, 999.9999999999998863 ) ;
#6694=CARTESIAN_POINT ( 'NONE',  ( 19.46461987976676511, 177.6255169206013989, 113.1985551865116406 ) ) ;
#6736=LINE ( 'NONE', #13762, #17944 ) ;
#6763=CARTESIAN_POINT ( 'NONE',  ( 13.85032138075246699, 137.5759562808229362, 104.3910387985238799 ) ) ;
#6788=VERTEX_POINT ( 'NONE', #1477 ) ;
#6816=DIRECTION ( 'NONE',  ( -0.01292394549866728373, -0.005513023399720296501, -0.9999012842304693116 ) ) ;
#6855=PLANE ( 'NONE',  #9527 ) ;
#6890=VERTEX_POINT ( 'NONE', #16416 ) ;
#6909=DIRECTION ( 'NONE',  ( -0.01292394549866728373, -0.005513023399720296501, -0.9999012842304693116 ) ) ;
#6935=CARTESIAN_POINT ( 'NONE',  ( -11.19281454843939194, 155.5569384583423300, 101.2152518466410243 ) ) ;
#6939=LINE ( 'NONE', #10291, #9175 ) ;
#6967=DIRECTION ( 'NONE',  ( 7.125109674160325297E-05, -0.9999848031710252272, 0.005512562950849327591 ) ) ;
#6972=DIRECTION ( 'NONE',  ( 0.01292394549866728373, 0.005513023399720296501, 0.9999012842304693116 ) ) ;
#7011=CARTESIAN_POINT ( 'NONE',  ( -16.82948163695635557, 175.4987477760657839, 90.67711988367965148 ) ) ;
#7070=LINE ( 'NONE', #19356, #9924 ) ;
#7076=CARTESIAN_POINT ( 'NONE',  ( 1.440275352545798748, 177.6144908738019694, 111.4313871723342544 ) ) ;
#7086=DIRECTION ( 'NONE',  ( 7.125109674160325297E-05, -0.9999848031710253382, 0.005512562950849327591 ) ) ;
#7087=AXIS2_PLACEMENT_3D ( 'NONE', #13268, #1082, #10035 ) ;
#7092=SHAPE_REPRESENTATION ( 'Square Thread Nut', ( #6292 ), #12539 ) ;
#7131=EDGE_CURVE ( 'NONE', #13046, #6788, #18764, .T. ) ;
#7167=DIRECTION ( 'NONE',  ( 0.5697992685214862130, 0.5741585497524474002, -0.5879377121248013927 ) ) ;
#7242=CYLINDRICAL_SURFACE ( 'NONE', #457, 8.000000000000000000 ) ;
#7245=DIRECTION ( 'NONE',  ( -0.01292394549866750231, -0.005513023399722823126, -0.9999012842304692006 ) ) ;
#7317=VECTOR ( 'NONE', #9260, 999.9999999999998863 ) ;
#7336=AXIS2_PLACEMENT_3D ( 'NONE', #6935, #183, #10743 ) ;
#7357=DIRECTION ( 'NONE',  ( 7.125109674160325297E-05, -0.9999848031710252272, 0.005512562950849327591 ) ) ;
#7363=LINE ( 'NONE', #12678, #16678 ) ;
#7406=DIRECTION ( 'NONE',  ( -0.009188991635466043154, 0.7031977391749434370, -0.7109349492407667226 ) ) ;
#7485=CARTESIAN_POINT ( 'NONE',  ( -14.55838832409743056, 177.6144908738019694, 111.6381734428085224 ) ) ;
#7488=DIRECTION ( 'NONE',  ( 0.9999164797902015955, 8.772500386246550856E-18, -0.01292414190464154927 ) ) ;
#7520=EDGE_CURVE ( 'NONE', #21699, #4461, #5391, .T. ) ;
#7553=ADVANCED_FACE ( 'NONE', ( #16013 ), #7242, .F. ) ;
#7579=ORIENTED_EDGE ( 'NONE', *, *, #22380, .T. ) ;
#7593=ORIENTED_EDGE ( 'NONE', *, *, #13721, .T. ) ;
#7629=VECTOR ( 'NONE', #294, 1000.000000000000114 ) ;
#7656=DIRECTION ( 'NONE',  ( 7.125109674160325297E-05, -0.9999848031710253382, 0.005512562950849327591 ) ) ;
#7668=VERTEX_POINT ( 'NONE', #3679 ) ;
#7676=CARTESIAN_POINT ( 'NONE',  ( -11.14759061400257423, 137.5759562808229362, 104.7141423461399086 ) ) ;
#7679=ORIENTED_EDGE ( 'NONE', *, *, #11556, .T. ) ;
#7682=EDGE_CURVE ( 'NONE', #3399, #5284, #11613, .T. ) ;
#7716=DIRECTION ( 'NONE',  ( -0.01104128644981280764, -0.5197558313507618655, -0.8542435049623797738 ) ) ;
#7762=CARTESIAN_POINT ( 'NONE',  ( 17.14168828271968437, 177.4876913356084174, 88.22687136455920154 ) ) ;
#7814=SHAPE_DEFINITION_REPRESENTATION ( #2770, #7092 ) ;
#7894=ORIENTED_EDGE ( 'NONE', *, *, #4435, .T. ) ;
#7896=CARTESIAN_POINT ( 'NONE',  ( 13.80509744631564750, 155.5569384583423300, 100.8921482990249956 ) ) ;
#7934=ORIENTED_EDGE ( 'NONE', *, *, #12164, .F. ) ;
#7945=ADVANCED_FACE ( 'NONE', ( #15412 ), #4848, .F. ) ;
#7992=EDGE_CURVE ( 'NONE', #14948, #638, #8474, .T. ) ;
#7997=VECTOR ( 'NONE', #14975, 999.9999999999998863 ) ;
#8004=ADVANCED_FACE ( 'NONE', ( #5367 ), #15983, .T. ) ;
#8057=EDGE_LOOP ( 'NONE', ( #6628, #5245, #11730, #1009, #3925, #5113, #18800, #20670 ) ) ;
#8062=CARTESIAN_POINT ( 'NONE',  ( 13.76115603162017820, 155.5381941787832716, 97.49248393264142010 ) ) ;
#8115=DIRECTION ( 'NONE',  ( -0.01292394549866728373, -0.005513023399720296501, -0.9999012842304693116 ) ) ;
#8218=AXIS2_PLACEMENT_3D ( 'NONE', #16129, #4023, #7488 ) ;
#8228=FACE_OUTER_BOUND ( 'NONE', #9121, .T. ) ;
#8277=EDGE_LOOP ( 'NONE', ( #9144, #13542, #14556, #11965 ) ) ;
#8279=CARTESIAN_POINT ( 'NONE',  ( -16.82962413914983912, 177.4987173824078468, 90.66609475777795524 ) ) ;
#8295=DIRECTION ( 'NONE',  ( 0.9999164797902017066, 0.000000000000000000, -0.01292414190464177826 ) ) ;
#8309=ORIENTED_EDGE ( 'NONE', *, *, #12603, .T. ) ;
#8377=DIRECTION ( 'NONE',  ( -7.125109674160325297E-05, 0.9999848031710253382, -0.005512562950849327591 ) ) ;
#8404=FACE_OUTER_BOUND ( 'NONE', #18039, .T. ) ;
#8437=DIRECTION ( 'NONE',  ( -0.01292394549866750231, -0.005513023399722823126, -0.9999012842304692006 ) ) ;
#8462=CIRCLE ( 'NONE', #2970, 3.399999999999991918 ) ;
#8465=CARTESIAN_POINT ( 'NONE',  ( 17.46478692018636636, 177.6255169206013989, 113.2244034703209365 ) ) ;
#8474=LINE ( 'NONE', #22472, #8526 ) ;
#8489=CYLINDRICAL_SURFACE ( 'NONE', #13706, 3.399999999999991918 ) ;
#8526=VECTOR ( 'NONE', #22580, 999.9999999999998863 ) ;
#8543=SURFACE_SIDE_STYLE ('',( #19743 ) ) ;
#8580=ORIENTED_EDGE ( 'NONE', *, *, #986, .F. ) ;
#8662=LINE ( 'NONE', #15951, #17278 ) ;
#8754=ORIENTED_EDGE ( 'NONE', *, *, #20423, .F. ) ;
#8773=EDGE_CURVE ( 'NONE', #22140, #6890, #11801, .T. ) ;
#8835=EDGE_CURVE ( 'NONE', #20077, #16143, #6939, .T. ) ;
#8855=CARTESIAN_POINT ( 'NONE',  ( -14.82979117956944037, 177.4987173824078468, 90.64024647396865930 ) ) ;
#8864=DIRECTION ( 'NONE',  ( -0.5698815422012539766, 0.5805244408402039369, 0.5815723527176038798 ) ) ;
#8872=ORIENTED_EDGE ( 'NONE', *, *, #4283, .F. ) ;
#8912=CARTESIAN_POINT ( 'NONE',  ( -6.855452219084264165, 165.4878736975560969, 88.60320152568080232 ) ) ;
#8915=CARTESIAN_POINT ( 'NONE',  ( 13.80637996605699769, 137.5572120012638777, 100.9913744321402902 ) ) ;
#8930=EDGE_LOOP ( 'NONE', ( #10507, #7593, #10925, #987 ) ) ;
#9017=ORIENTED_EDGE ( 'NONE', *, *, #14235, .F. ) ;
#9018=DIRECTION ( 'NONE',  ( 0.01292394549866728373, 0.005513023399720296501, 0.9999012842304693116 ) ) ;
#9042=ORIENTED_EDGE ( 'NONE', *, *, #6130, .F. ) ;
#9053=CARTESIAN_POINT ( 'NONE',  ( -11.23547344339351284, 137.5384677217048193, 97.91481361337272915 ) ) ;
#9065=CARTESIAN_POINT ( 'NONE',  ( -14.53239793090661180, 175.6255473142593644, 113.6490011371711688 ) ) ;
#9121=EDGE_LOOP ( 'NONE', ( #19201, #4156, #9793, #9745 ) ) ;
#9144=ORIENTED_EDGE ( 'NONE', *, *, #2229, .F. ) ;
#9157=PRODUCT_DEFINITION ( 'UNKNOWN', '', #21273, #12717 ) ;
#9175=VECTOR ( 'NONE', #17304, 1000.000000000000114 ) ;
#9188=CARTESIAN_POINT ( 'NONE',  ( 1.143866695291850588, 165.4878681845327151, 88.49880848915942977 ) ) ;
#9189=FILL_AREA_STYLE_COLOUR ( '', #17978 ) ;
#9195=VECTOR ( 'NONE', #7086, 999.9999999999998863 ) ;
#9198=CARTESIAN_POINT ( 'NONE',  ( 1.143879619237349266, 165.4878736975560969, 88.49980839044366121 ) ) ;
#9237=FACE_OUTER_BOUND ( 'NONE', #4762, .T. ) ;
#9253=EDGE_CURVE ( 'NONE', #6890, #11929, #19369, .T. ) ;
#9260=DIRECTION ( 'NONE',  ( 7.125109674160325297E-05, -0.9999848031710253382, 0.005512562950849327591 ) ) ;
#9310=EDGE_LOOP ( 'NONE', ( #17602, #5418, #9628 ) ) ;
#9334=ORIENTED_EDGE ( 'NONE', *, *, #16777, .F. ) ;
#9351=CARTESIAN_POINT ( 'NONE',  ( 19.43877198876942813, 177.6144908738019694, 111.1987526180507047 ) ) ;
#9358=ORIENTED_EDGE ( 'NONE', *, *, #3086, .T. ) ;
#9365=DIRECTION ( 'NONE',  ( -0.9999164797902015955, -8.772500386246549315E-18, 0.01292414190464155101 ) ) ;
#9373=EDGE_LOOP ( 'NONE', ( #6452, #7894, #8754 ) ) ;
#9414=DIRECTION ( 'NONE',  ( -0.7161863329816251511, -0.003898296230782250828, -0.6978982302147139771 ) ) ;
#9474=AXIS2_PLACEMENT_3D ( 'NONE', #3836, #7167, #45 ) ;
#9478=EDGE_CURVE ( 'NONE', #6890, #16183, #8462, .T. ) ;
#9527=AXIS2_PLACEMENT_3D ( 'NONE', #1706, #10653, #6972 ) ;
#9583=CARTESIAN_POINT ( 'NONE',  ( 13.80637996605699769, 137.5572120012638777, 100.9913744321402902 ) ) ;
#9628=ORIENTED_EDGE ( 'NONE', *, *, #12205, .T. ) ;
#9678=LINE ( 'NONE', #16370, #14808 ) ;
#9692=CARTESIAN_POINT ( 'NONE',  ( 17.14183078491316436, 175.4877217292663545, 88.23789649046089778 ) ) ;
#9696=LINE ( 'NONE', #16720, #15741 ) ;
#9707=VECTOR ( 'NONE', #1583, 999.9999999999998863 ) ;
#9715=CIRCLE ( 'NONE', #1275, 3.399999999999991918 ) ;
#9745=ORIENTED_EDGE ( 'NONE', *, *, #11185, .T. ) ;
#9746=ORIENTED_EDGE ( 'NONE', *, *, #16777, .T. ) ;
#9763=ORIENTED_EDGE ( 'NONE', *, *, #11452, .T. ) ;
#9793=ORIENTED_EDGE ( 'NONE', *, *, #20455, .T. ) ;
#9798=CARTESIAN_POINT ( 'NONE',  ( -16.82962413914983912, 177.4987173824078468, 90.66609475777795524 ) ) ;
#9881=LINE ( 'NONE', #4685, #4548 ) ;
#9890=VECTOR ( 'NONE', #14518, 1000.000000000000114 ) ;
#9895=VECTOR ( 'NONE', #14388, 999.9999999999998863 ) ;
#9924=VECTOR ( 'NONE', #3514, 999.9999999999998863 ) ;
#10005=ORIENTED_EDGE ( 'NONE', *, *, #20718, .F. ) ;
#10035=DIRECTION ( 'NONE',  ( 0.01292394549866728373, 0.005513023399720296501, 0.9999012842304693116 ) ) ;
#10079=VERTEX_POINT ( 'NONE', #3996 ) ;
#10123=DIRECTION ( 'NONE',  ( -0.9999164797902015955, -8.506845633049209592E-18, 0.01292414190464159611 ) ) ;
#10159=CARTESIAN_POINT ( 'NONE',  ( -16.85532952795369255, 175.4877217292663545, 88.67731731521871552 ) ) ;
#10218=DIRECTION ( 'NONE',  ( 7.125109674160325297E-05, -0.9999848031710253382, 0.005512562950849327591 ) ) ;
#10242=ORIENTED_EDGE ( 'NONE', *, *, #7682, .T. ) ;
#10266=ORIENTED_EDGE ( 'NONE', *, *, #4435, .F. ) ;
#10286=CONICAL_SURFACE ( 'NONE', #7336, 3.399999999999991918, 1.029744258676652313 ) ;
#10291=CARTESIAN_POINT ( 'NONE',  ( 19.44162203263909205, 137.6150987469609674, 111.4192551360846863 ) ) ;
#10312=LINE ( 'NONE', #1702, #167 ) ;
#10365=VERTEX_POINT ( 'NONE', #2431 ) ;
#10433=VECTOR ( 'NONE', #6816, 999.9999999999998863 ) ;
#10485=CARTESIAN_POINT ( 'NONE',  ( 19.44162203263909205, 137.6150987469609674, 111.4192551360846863 ) ) ;
#10493=PLANE ( 'NONE',  #2687 ) ;
#10503=ORIENTED_EDGE ( 'NONE', *, *, #3503, .F. ) ;
#10507=ORIENTED_EDGE ( 'NONE', *, *, #14030, .T. ) ;
#10546=CARTESIAN_POINT ( 'NONE',  ( 19.14166374449356312, 175.4877217292663545, 88.21204820665161606 ) ) ;
#10627=VERTEX_POINT ( 'NONE', #14020 ) ;
#10653=DIRECTION ( 'NONE',  ( 0.7069973413461614342, 0.7070960354057256314, -0.01303671902605248872 ) ) ;
#10740=CARTESIAN_POINT ( 'NONE',  ( -14.53239793090661180, 175.6255473142593644, 113.6490011371711688 ) ) ;
#10743=DIRECTION ( 'NONE',  ( -0.01292394549866750231, -0.005513023399722823126, -0.9999012842304692006 ) ) ;
#10785=VERTEX_POINT ( 'NONE', #14922 ) ;
#10811=ORIENTED_EDGE ( 'NONE', *, *, #14235, .T. ) ;
#10870=FACE_OUTER_BOUND ( 'NONE', #11743, .T. ) ;
#10911=EDGE_LOOP ( 'NONE', ( #10005, #10503, #9017, #13135 ) ) ;
#10925=ORIENTED_EDGE ( 'NONE', *, *, #986, .T. ) ;
#10963=FACE_OUTER_BOUND ( 'NONE', #13066, .T. ) ;
#10994=ORIENTED_EDGE ( 'NONE', *, *, #2126, .F. ) ;
#10997=LINE ( 'NONE', #2046, #4022 ) ;
#11013=VERTEX_POINT ( 'NONE', #10740 ) ;
#11070=EDGE_LOOP ( 'NONE', ( #18583, #6459, #18896, #18677 ) ) ;
#11095=AXIS2_PLACEMENT_3D ( 'NONE', #16074, #12389, #14346 ) ;
#11113=EDGE_CURVE ( 'NONE', #20395, #3828, #20296, .T. ) ;
#11117=DIRECTION ( 'NONE',  ( -0.01292394549866750231, -0.005513023399722823126, -0.9999012842304692006 ) ) ;
#11165=DIRECTION ( 'NONE',  ( 0.01292394549866728373, 0.005513023399720296501, 0.9999012842304693116 ) ) ;
#11185=EDGE_CURVE ( 'NONE', #17187, #14649, #13365, .T. ) ;
#11202=ADVANCED_FACE ( 'NONE', ( #15109 ), #18641, .T. ) ;
#11324=PLANE ( 'NONE',  #17772 ) ;
#11452=EDGE_CURVE ( 'NONE', #638, #16185, #15561, .T. ) ;
#11455=VECTOR ( 'NONE', #2997, 1000.000000000000227 ) ;
#11488=ADVANCED_FACE ( 'NONE', ( #13026, #5642 ), #19752, .F. ) ;
#11516=DIRECTION ( 'NONE',  ( -0.01292394549866750231, -0.005513023399722823126, -0.9999012842304692006 ) ) ;
#11523=AXIS2_PLACEMENT_3D ( 'NONE', #19082, #7357, #7245 ) ;
#11547=CARTESIAN_POINT ( 'NONE',  ( -16.55807878148434753, 175.6145212674599065, 111.6750468525195004 ) ) ;
#11556=EDGE_CURVE ( 'NONE', #5939, #14141, #2343, .T. ) ;
#11572=ORIENTED_EDGE ( 'NONE', *, *, #21604, .F. ) ;
#11600=EDGE_CURVE ( 'NONE', #16835, #21699, #7363, .T. ) ;
#11606=ORIENTED_EDGE ( 'NONE', *, *, #12588, .T. ) ;
#11613=LINE ( 'NONE', #15068, #12206 ) ;
#11624=ADVANCED_FACE ( 'NONE', ( #1295 ), #17030, .F. ) ;
#11686=CONICAL_SURFACE ( 'NONE', #17925, 3.399999999999991918, 1.029744258676652313 ) ;
#11702=CARTESIAN_POINT ( 'NONE',  ( -11.19153202869804353, 137.5572120012638777, 101.3144779797563189 ) ) ;
#11730=ORIENTED_EDGE ( 'NONE', *, *, #22245, .F. ) ;
#11743=EDGE_LOOP ( 'NONE', ( #11572, #8580, #8872, #9334 ) ) ;
#11771=ORIENTED_EDGE ( 'NONE', *, *, #3086, .F. ) ;
#11785=AXIS2_PLACEMENT_3D ( 'NONE', #21187, #7406, #5672 ) ;
#11801=LINE ( 'NONE', #3057, #4770 ) ;
#11802=DIRECTION ( 'NONE',  ( 7.125109674160325297E-05, -0.9999848031710252272, 0.005512562950849327591 ) ) ;
#11825=VECTOR ( 'NONE', #15774, 1000.000000000000114 ) ;
#11855=ORIENTED_EDGE ( 'NONE', *, *, #2126, .T. ) ;
#11919=CYLINDRICAL_SURFACE ( 'NONE', #16570, 3.399999999999991918 ) ;
#11929=VERTEX_POINT ( 'NONE', #7676 ) ;
#11959=ORIENTED_EDGE ( 'NONE', *, *, #7131, .T. ) ;
#11965=ORIENTED_EDGE ( 'NONE', *, *, #15355, .F. ) ;
#11987=DIRECTION ( 'NONE',  ( 0.01292394549866728373, 0.005513023399720296501, 0.9999012842304693116 ) ) ;
#12007=PRESENTATION_STYLE_ASSIGNMENT (( #22533 ) ) ;
#12025=DIRECTION ( 'NONE',  ( 0.7161863329816251511, 0.003898296230782347105, 0.6978982302147139771 ) ) ;
#12050=CARTESIAN_POINT ( 'NONE',  ( -14.52969038923042966, 137.6261247937603969, 113.8584785293034400 ) ) ;
#12069=DIRECTION ( 'NONE',  ( 0.000000000000000000, 0.000000000000000000, 1.000000000000000000 ) ) ;
#12073=FACE_BOUND ( 'NONE', #17915, .T. ) ;
#12164=EDGE_CURVE ( 'NONE', #14649, #17187, #9715, .T. ) ;
#12179=CARTESIAN_POINT ( 'NONE',  ( 13.80509744631564750, 155.5569384583423300, 100.8921482990249956 ) ) ;
#12205=EDGE_CURVE ( 'NONE', #3828, #20395, #4182, .T. ) ;
#12206=VECTOR ( 'NONE', #2538, 1000.000000000000114 ) ;
#12221=DIRECTION ( 'NONE',  ( -7.125109674160325297E-05, 0.9999848031710253382, -0.005512562950849327591 ) ) ;
#12235=EDGE_CURVE ( 'NONE', #14141, #6788, #10312, .T. ) ;
#12245=AXIS2_PLACEMENT_3D ( 'NONE', #3623, #21309, #1918 ) ;
#12326=ORIENTED_EDGE ( 'NONE', *, *, #9253, .F. ) ;
#12353=ADVANCED_FACE ( 'NONE', ( #21865 ), #4424, .F. ) ;
#12389=DIRECTION ( 'NONE',  ( -0.5848048290265493998, 0.5741585497524471782, -0.5730141985094219237 ) ) ;
#12391=DIRECTION ( 'NONE',  ( -0.01292394549866750231, -0.005513023399722823126, -0.9999012842304692006 ) ) ;
#12398=DIRECTION ( 'NONE',  ( 0.9999164797902015955, 8.772500386246549315E-18, -0.01292414190464155101 ) ) ;
#12453=ORIENTED_EDGE ( 'NONE', *, *, #11556, .F. ) ;
#12457=ADVANCED_FACE ( 'NONE', ( #14288 ), #10493, .T. ) ;
#12486=DIRECTION ( 'NONE',  ( 0.009088227368120111588, 0.7109943316365107124, 0.7031390079522377157 ) ) ;
#12515=CARTESIAN_POINT ( 'NONE',  ( -11.19296010916491824, 157.5998335170374389, 101.2039900878849750 ) ) ;
#12539=( GEOMETRIC_REPRESENTATION_CONTEXT ( 3 ) GLOBAL_UNCERTAINTY_ASSIGNED_CONTEXT ( ( #22522 ) ) GLOBAL_UNIT_ASSIGNED_CONTEXT ( ( #5775, #631, #14664 ) ) REPRESENTATION_CONTEXT ( 'NONE', 'WORKASPACE' ) );
#12588=EDGE_CURVE ( 'NONE', #22140, #16183, #9678, .T. ) ;
#12603=EDGE_CURVE ( 'NONE', #14141, #5939, #1564, .T. ) ;
#12608=FACE_OUTER_BOUND ( 'NONE', #5734, .T. ) ;
#12636=AXIS2_PLACEMENT_3D ( 'NONE', #9198, #19871, #5747 ) ;
#12660=VECTOR ( 'NONE', #1485, 1000.000000000000114 ) ;
#12664=PRODUCT_CONTEXT ( 'NONE', #22277, 'mechanical' ) ;
#12678=CARTESIAN_POINT ( 'NONE',  ( -14.85563907056677913, 177.4876913356084174, 88.64044390550773755 ) ) ;
#12694=ORIENTED_EDGE ( 'NONE', *, *, #22523, .F. ) ;
#12706=DIRECTION ( 'NONE',  ( 0.9999164797902017066, 0.000000000000000000, -0.01292414190464177826 ) ) ;
#12717=PRODUCT_DEFINITION_CONTEXT ( 'detailed design', #1916, 'design' ) ;
#12781=ADVANCED_FACE ( 'NONE', ( #13574 ), #8489, .F. ) ;
#12822=LINE ( 'NONE', #18003, #13670 ) ;
#12871=ADVANCED_FACE ( 'NONE', ( #17480 ), #14154, .F. ) ;
#12888=VECTOR ( 'NONE', #11165, 999.9999999999998863 ) ;
#12895=CARTESIAN_POINT ( 'NONE',  ( 19.16751163549090009, 175.4987477760657839, 90.21185077511255201 ) ) ;
#13026=FACE_BOUND ( 'NONE', #13868, .T. ) ;
#13039=PLANE ( 'NONE',  #5784 ) ;
#13046=VERTEX_POINT ( 'NONE', #3068 ) ;
#13057=DIRECTION ( 'NONE',  ( -0.7161863329816273716, -0.003898296230782334528, -0.6978982302147116457 ) ) ;
#13066=EDGE_LOOP ( 'NONE', ( #18090, #20063, #20889 ) ) ;
#13135=ORIENTED_EDGE ( 'NONE', *, *, #11600, .F. ) ;
#13146=ADVANCED_FACE ( 'NONE', ( #10870 ), #20848, .T. ) ;
#13153=DIRECTION ( 'NONE',  ( -0.01292394549866750231, -0.005513023399722823126, -0.9999012842304692006 ) ) ;
#13169=VECTOR ( 'NONE', #4382, 1000.000000000000114 ) ;
#13172=DIRECTION ( 'NONE',  ( -0.01292394549866728373, -0.005513023399720296501, -0.9999012842304693116 ) ) ;
#13217=ADVANCED_FACE ( 'NONE', ( #18321 ), #11324, .F. ) ;
#13268=CARTESIAN_POINT ( 'NONE',  ( 1.304573924809790730, 177.5566041281049081, 100.9324236879143371 ) ) ;
#13365=CIRCLE ( 'NONE', #3433, 3.399999999999991918 ) ;
#13375=LINE ( 'NONE', #856, #16320 ) ;
#13513=( NAMED_UNIT ( * ) PLANE_ANGLE_UNIT ( ) SI_UNIT ( $, .RADIAN. ) );
#13542=ORIENTED_EDGE ( 'NONE', *, *, #3620, .F. ) ;
#13545=DIRECTION ( 'NONE',  ( 7.125109674160325297E-05, -0.9999848031710252272, 0.005512562950849327591 ) ) ;
#13568=DIRECTION ( 'NONE',  ( 0.7161863329816273716, 0.003898296230782334528, 0.6978982302147116457 ) ) ;
#13571=VECTOR ( 'NONE', #9018, 999.9999999999998863 ) ;
#13574=FACE_OUTER_BOUND ( 'NONE', #20740, .T. ) ;
#13670=VECTOR ( 'NONE', #9365, 1000.000000000000227 ) ;
#13706=AXIS2_PLACEMENT_3D ( 'NONE', #20219, #4486, #11516 ) ;
#13721=EDGE_CURVE ( 'NONE', #16143, #10785, #1379, .T. ) ;
#13745=CARTESIAN_POINT ( 'NONE',  ( -16.53223089048701056, 175.6255473142593644, 113.6748494209804363 ) ) ;
#13762=CARTESIAN_POINT ( 'NONE',  ( 17.14453832658934829, 137.4882992087673870, 88.44737388259316901 ) ) ;
#13855=FACE_OUTER_BOUND ( 'NONE', #4535, .T. ) ;
#13868=EDGE_LOOP ( 'NONE', ( #324, #12453 ) ) ;
#13894=DIRECTION ( 'NONE',  ( -0.01292394549866750231, -0.005513023399722823126, -0.9999012842304692006 ) ) ;
#13918=ORIENTED_EDGE ( 'NONE', *, *, #22380, .F. ) ;
#14018=VECTOR ( 'NONE', #18064, 999.9999999999998863 ) ;
#14020=CARTESIAN_POINT ( 'NONE',  ( 17.14453832658934829, 137.4882992087673870, 88.44737388259316901 ) ) ;
#14030=EDGE_CURVE ( 'NONE', #14948, #16143, #13375, .T. ) ;
#14078=EDGE_CURVE ( 'NONE', #3399, #4461, #4497, .T. ) ;
#14095=CARTESIAN_POINT ( 'NONE',  ( -11.19281454843939194, 155.5569384583423300, 101.2152518466410243 ) ) ;
#14110=ORIENTED_EDGE ( 'NONE', *, *, #14479, .T. ) ;
#14111=VERTEX_POINT ( 'NONE', #7011 ) ;
#14139=DIRECTION ( 'NONE',  ( 0.5847225553467816361, 0.5805244408402039369, 0.5666488391022245219 ) ) ;
#14141=VERTEX_POINT ( 'NONE', #17212 ) ;
#14154=CYLINDRICAL_SURFACE ( 'NONE', #5619, 3.399999999999991918 ) ;
#14179=EDGE_LOOP ( 'NONE', ( #1310, #10994, #2288, #21473 ) ) ;
#14212=PLANE ( 'NONE',  #11785 ) ;
#14235=EDGE_CURVE ( 'NONE', #21699, #14111, #3642, .T. ) ;
#14287=ORIENTED_EDGE ( 'NONE', *, *, #15355, .T. ) ;
#14288=FACE_OUTER_BOUND ( 'NONE', #20784, .T. ) ;
#14304=EDGE_LOOP ( 'NONE', ( #17441, #21456, #19600 ) ) ;
#14346=DIRECTION ( 'NONE',  ( -0.6979091139780387865, 0.003898296230782335829, 0.7161757269782926816 ) ) ;
#14366=CARTESIAN_POINT ( 'NONE',  ( 19.43891449096291169, 175.6145212674599065, 111.2097777439524151 ) ) ;
#14388=DIRECTION ( 'NONE',  ( 7.125109674160325297E-05, -0.9999848031710253382, 0.005512562950849327591 ) ) ;
#14428=LINE ( 'NONE', #19104, #18305 ) ;
#14471=VECTOR ( 'NONE', #10218, 999.9999999999998863 ) ;
#14479=EDGE_CURVE ( 'NONE', #16185, #14111, #3373, .T. ) ;
#14518=DIRECTION ( 'NONE',  ( 0.7069973413461587697, 0.7070960354057281849, -0.01303671902605484795 ) ) ;
#14530=FACE_BOUND ( 'NONE', #3582, .T. ) ;
#14556=ORIENTED_EDGE ( 'NONE', *, *, #4557, .F. ) ;
#14649=VERTEX_POINT ( 'NONE', #14764 ) ;
#14664=( NAMED_UNIT ( * ) SI_UNIT ( $, .STERADIAN. ) SOLID_ANGLE_UNIT ( ) );
#14686=STYLED_ITEM ( 'NONE', ( #12007 ), #17421 ) ;
#14764=CARTESIAN_POINT ( 'NONE',  ( 13.85032138075246699, 137.5759562808229362, 104.3910387985238799 ) ) ;
#14808=VECTOR ( 'NONE', #7716, 1000.000000000000114 ) ;
#14837=AXIS2_PLACEMENT_3D ( 'NONE', #7076, #12486, #195 ) ;
#14850=ORIENTED_EDGE ( 'NONE', *, *, #14078, .F. ) ;
#14905=ORIENTED_EDGE ( 'NONE', *, *, #5913, .T. ) ;
#14922=CARTESIAN_POINT ( 'NONE',  ( 17.46492942237984991, 175.6255473142593644, 113.2354285962226328 ) ) ;
#14948=VERTEX_POINT ( 'NONE', #12050 ) ;
#14975=DIRECTION ( 'NONE',  ( 7.125109674160325297E-05, -0.9999848031710253382, 0.005512562950849327591 ) ) ;
#15063=VERTEX_POINT ( 'NONE', #21449 ) ;
#15068=CARTESIAN_POINT ( 'NONE',  ( 18.16752390460396072, 176.4987325792368154, 90.21926235406634476 ) ) ;
#15109=FACE_OUTER_BOUND ( 'NONE', #17827, .T. ) ;
#15128=AXIS2_PLACEMENT_3D ( 'NONE', #1508, #6552, #10123 ) ;
#15223=CYLINDRICAL_SURFACE ( 'NONE', #2143, 8.000000000000000000 ) ;
#15238=LINE ( 'NONE', #16946, #6267 ) ;
#15306=CARTESIAN_POINT ( 'NONE',  ( -16.55537123980816716, 137.6150987469609674, 111.8845242446517858 ) ) ;
#15352=EDGE_CURVE ( 'NONE', #11013, #14948, #7070, .T. ) ;
#15355=EDGE_CURVE ( 'NONE', #15063, #5284, #8662, .T. ) ;
#15407=ORIENTED_EDGE ( 'NONE', *, *, #4998, .T. ) ;
#15412=FACE_OUTER_BOUND ( 'NONE', #14304, .T. ) ;
#15427=ORIENTED_EDGE ( 'NONE', *, *, #18497, .T. ) ;
#15448=PLANE ( 'NONE',  #18007 ) ;
#15486=FACE_OUTER_BOUND ( 'NONE', #17482, .T. ) ;
#15561=LINE ( 'NONE', #15906, #1262 ) ;
#15669=CARTESIAN_POINT ( 'NONE',  ( -14.69408975183343635, 177.5566041281049081, 101.1392099583886051 ) ) ;
#15703=ORIENTED_EDGE ( 'NONE', *, *, #16113, .F. ) ;
#15741=VECTOR ( 'NONE', #22057, 1000.000000000000114 ) ;
#15744=LINE ( 'NONE', #6763, #14471 ) ;
#15774=DIRECTION ( 'NONE',  ( -0.009188991635465687535, 0.7031977391749432149, -0.7109349492407668336 ) ) ;
#15828=AXIS2_PLACEMENT_3D ( 'NONE', #4759, #11802, #8437 ) ;
#15890=AXIS2_PLACEMENT_3D ( 'NONE', #12179, #17351, #13894 ) ;
#15894=ORIENTED_EDGE ( 'NONE', *, *, #7131, .F. ) ;
#15906=CARTESIAN_POINT ( 'NONE',  ( -16.55822128367782753, 177.6144908738019694, 111.6640217266178041 ) ) ;
#15911=ORIENTED_EDGE ( 'NONE', *, *, #12235, .F. ) ;
#15951=CARTESIAN_POINT ( 'NONE',  ( 19.16736913329742009, 177.4987173824078468, 90.20082564921086998 ) ) ;
#15983=PLANE ( 'NONE',  #5592 ) ;
#15996=ADVANCED_FACE ( 'NONE', ( #13855 ), #16945, .F. ) ;
#15998=CARTESIAN_POINT ( 'NONE',  ( 13.80637996605699769, 137.5572120012638777, 100.9913744321402902 ) ) ;
#16001=ADVANCED_FACE ( 'NONE', ( #15486 ), #11919, .F. ) ;
#16011=ORIENTED_EDGE ( 'NONE', *, *, #1278, .T. ) ;
#16013=FACE_OUTER_BOUND ( 'NONE', #3445, .T. ) ;
#16046=PRODUCT ( 'Square Thread Nut', 'Square Thread Nut', '', ( #12664 ) ) ;
#16073=LINE ( 'NONE', #21315, #7317 ) ;
#16074=CARTESIAN_POINT ( 'NONE',  ( -14.82979117956944037, 177.4987173824078468, 90.64024647396865930 ) ) ;
#16113=EDGE_CURVE ( 'NONE', #16183, #6890, #5162, .T. ) ;
#16129=CARTESIAN_POINT ( 'NONE',  ( 19.14152124230007956, 177.4876913356084174, 88.20102308074991981 ) ) ;
#16134=ADVANCED_FACE ( 'NONE', ( #9237 ), #14212, .T. ) ;
#16143=VERTEX_POINT ( 'NONE', #5441 ) ;
#16153=CARTESIAN_POINT ( 'NONE',  ( 1.466978256704031480, 165.6256992825491068, 113.4973404962053820 ) ) ;
#16161=CARTESIAN_POINT ( 'NONE',  ( 1.466978256704031480, 165.6256992825491068, 113.4973404962053820 ) ) ;
#16183=VERTEX_POINT ( 'NONE', #21737 ) ;
#16185=VERTEX_POINT ( 'NONE', #11547 ) ;
#16320=VECTOR ( 'NONE', #4375, 1000.000000000000227 ) ;
#16357=CARTESIAN_POINT ( 'NONE',  ( -16.52952334881082663, 137.6261247937603969, 113.8843268131127218 ) ) ;
#16370=CARTESIAN_POINT ( 'NONE',  ( -11.23675596313486125, 155.5381941787832716, 97.81558748025743455 ) ) ;
#16373=DIRECTION ( 'NONE',  ( -0.01292394549866750231, -0.005513023399722823126, -0.9999012842304692006 ) ) ;
#16416=CARTESIAN_POINT ( 'NONE',  ( -11.14887313374392264, 155.5756827379013885, 104.6149162130246282 ) ) ;
#16523=CARTESIAN_POINT ( 'NONE',  ( -11.19281454843939194, 155.5569384583423300, 101.2152518466410243 ) ) ;
#16570=AXIS2_PLACEMENT_3D ( 'NONE', #5096, #18900, #22440 ) ;
#16633=LINE ( 'NONE', #6149, #6621 ) ;
#16678=VECTOR ( 'NONE', #8377, 999.9999999999998863 ) ;
#16710=CARTESIAN_POINT ( 'NONE',  ( 1.307423968679454873, 137.5572120012638777, 101.1529262059483045 ) ) ;
#16720=CARTESIAN_POINT ( 'NONE',  ( 17.45193422578444142, 176.6200190940306527, 112.2300147490413167 ) ) ;
#16746=ORIENTED_EDGE ( 'NONE', *, *, #15352, .F. ) ;
#16768=DIRECTION ( 'NONE',  ( -0.9999164797902015955, -8.506845633049208051E-18, 0.01292414190464159611 ) ) ;
#16777=EDGE_CURVE ( 'NONE', #5296, #7668, #1186, .T. ) ;
#16788=ORIENTED_EDGE ( 'NONE', *, *, #5913, .F. ) ;
#16807=ADVANCED_FACE ( 'NONE', ( #17930 ), #5719, .T. ) ;
#16835=VERTEX_POINT ( 'NONE', #18043 ) ;
#16945=CONICAL_SURFACE ( 'NONE', #15828, 3.399999999999991918, 1.029744258676652313 ) ;
#16946=CARTESIAN_POINT ( 'NONE',  ( 13.84903886101111681, 155.5756827379013885, 104.2918126654085853 ) ) ;
#16976=DIRECTION ( 'NONE',  ( 7.125109674160325297E-05, -0.9999848031710252272, 0.005512562950849327591 ) ) ;
#16995=AXIS2_PLACEMENT_3D ( 'NONE', #17965, #19758, #18290 ) ;
#17030=PLANE ( 'NONE',  #898 ) ;
#17051=AXIS2_PLACEMENT_3D ( 'NONE', #17205, #19139, #12391 ) ;
#17063=DIRECTION ( 'NONE',  ( 0.01111468050521496539, -0.5103046645782702839, 0.8599218645824316942 ) ) ;
#17096=ADVANCED_FACE ( 'NONE', ( #22336 ), #17905, .T. ) ;
#17187=VERTEX_POINT ( 'NONE', #3954 ) ;
#17198=VECTOR ( 'NONE', #9414, 1000.000000000000000 ) ;
#17205=CARTESIAN_POINT ( 'NONE',  ( 13.80509744631564750, 155.5569384583423300, 100.8921482990249956 ) ) ;
#17212=CARTESIAN_POINT ( 'NONE',  ( 9.143211457558962252, 165.4878736975560969, 88.39641525520653431 ) ) ;
#17219=AXIS2_PLACEMENT_3D ( 'NONE', #11702, #13545, #18695 ) ;
#17238=PLANE ( 'NONE',  #15128 ) ;
#17278=VECTOR ( 'NONE', #1574, 999.9999999999998863 ) ;
#17301=CYLINDRICAL_SURFACE ( 'NONE', #17802, 3.399999999999991918 ) ;
#17304=DIRECTION ( 'NONE',  ( -0.6979091139780387865, 0.003898296230782336263, 0.7161757269782926816 ) ) ;
#17351=DIRECTION ( 'NONE',  ( 7.125109674160325297E-05, -0.9999848031710252272, 0.005512562950849327591 ) ) ;
#17364=DIRECTION ( 'NONE',  ( -0.01292394549866750231, -0.005513023399722823126, -0.9999012842304692006 ) ) ;
#17421=MANIFOLD_SOLID_BREP ( 'Stock-MAS-425-1', #1947 ) ;
#17441=ORIENTED_EDGE ( 'NONE', *, *, #6410, .F. ) ;
#17480=FACE_OUTER_BOUND ( 'NONE', #11070, .T. ) ;
#17482=EDGE_LOOP ( 'NONE', ( #12326, #15703, #9358, #22597 ) ) ;
#17593=VECTOR ( 'NONE', #2007, 1000.000000000000114 ) ;
#17602=ORIENTED_EDGE ( 'NONE', *, *, #4275, .F. ) ;
#17617=DIRECTION ( 'NONE',  ( -0.7069973413461592138, -0.7070960354057278519, 0.01303671902605246964 ) ) ;
#17642=CIRCLE ( 'NONE', #5878, 8.000000000000000000 ) ;
#17691=CARTESIAN_POINT ( 'NONE',  ( 17.16753617371702134, 177.4987173824078468, 90.22667393302013750 ) ) ;
#17729=FILL_AREA_STYLE ('',( #9189 ) ) ;
#17748=CARTESIAN_POINT ( 'NONE',  ( -14.53239793090661180, 175.6255473142593644, 113.6490011371711688 ) ) ;
#17772=AXIS2_PLACEMENT_3D ( 'NONE', #7762, #991, #6151 ) ;
#17781=ORIENTED_EDGE ( 'NONE', *, *, #5250, .T. ) ;
#17792=LINE ( 'NONE', #3863, #13571 ) ;
#17796=DIRECTION ( 'NONE',  ( 0.6979091139780387865, -0.003898296230782336263, -0.7161757269782926816 ) ) ;
#17802=AXIS2_PLACEMENT_3D ( 'NONE', #22312, #16976, #4750 ) ;
#17827=EDGE_LOOP ( 'NONE', ( #16011, #1919, #7579, #9746 ) ) ;
#17837=LINE ( 'NONE', #9053, #9895 ) ;
#17861=ADVANCED_FACE ( 'NONE', ( #8404 ), #15448, .F. ) ;
#17876=DIRECTION ( 'NONE',  ( 0.9999164797902017066, 0.000000000000000000, -0.01292414190464177826 ) ) ;
#17905=PLANE ( 'NONE',  #11095 ) ;
#17915=EDGE_LOOP ( 'NONE', ( #9042, #15894 ) ) ;
#17925=AXIS2_PLACEMENT_3D ( 'NONE', #7896, #19996, #16373 ) ;
#17930=FACE_OUTER_BOUND ( 'NONE', #21131, .T. ) ;
#17944=VECTOR ( 'NONE', #12025, 1000.000000000000000 ) ;
#17951=DIRECTION ( 'NONE',  ( 0.9999164797902017066, 0.000000000000000000, -0.01292414190464177826 ) ) ;
#17965=CARTESIAN_POINT ( 'NONE',  ( 1.143879619237349266, 165.4878736975560969, 88.49980839044366121 ) ) ;
#17971=ADVANCED_FACE ( 'NONE', ( #12073, #4932 ), #17238, .F. ) ;
#17978=COLOUR_RGB ( '', 0.40784314, 0.44705882, 0.49803922) ;
#18003=CARTESIAN_POINT ( 'NONE',  ( 19.14437128616974348, 137.4882992087673870, 88.42152559878388729 ) ) ;
#18007=AXIS2_PLACEMENT_3D ( 'NONE', #6694, #4955, #11987 ) ;
#18039=EDGE_LOOP ( 'NONE', ( #1470, #14287, #11855, #14905 ) ) ;
#18043=CARTESIAN_POINT ( 'NONE',  ( -14.85278902669711520, 137.4882992087673870, 88.86094642354169082 ) ) ;
#18064=DIRECTION ( 'NONE',  ( 0.01292394549866728373, 0.005513023399720296501, 0.9999012842304693116 ) ) ;
#18090=ORIENTED_EDGE ( 'NONE', *, *, #12588, .F. ) ;
#18212=DIRECTION ( 'NONE',  ( -0.01292394549866750231, -0.005513023399722823126, -0.9999012842304692006 ) ) ;
#18262=ORIENTED_EDGE ( 'NONE', *, *, #7520, .F. ) ;
#18290=DIRECTION ( 'NONE',  ( 0.9999164797902017066, 0.000000000000000000, -0.01292414190464177826 ) ) ;
#18294=CARTESIAN_POINT ( 'NONE',  ( 17.14168828271968437, 177.4876913356084174, 88.22687136455920154 ) ) ;
#18305=VECTOR ( 'NONE', #1885, 999.9999999999998863 ) ;
#18321=FACE_OUTER_BOUND ( 'NONE', #8277, .T. ) ;
#18440=ORIENTED_EDGE ( 'NONE', *, *, #13721, .F. ) ;
#18497=EDGE_CURVE ( 'NONE', #10627, #16835, #12822, .T. ) ;
#18514=CARTESIAN_POINT ( 'NONE',  ( -14.53239793090661180, 175.6255473142593644, 113.6490011371711688 ) ) ;
#18542=ORIENTED_EDGE ( 'NONE', *, *, #4719, .T. ) ;
#18564=( LENGTH_UNIT ( ) NAMED_UNIT ( * ) SI_UNIT ( .MILLI., .METRE. ) );
#18583=ORIENTED_EDGE ( 'NONE', *, *, #12205, .F. ) ;
#18591=ORIENTED_EDGE ( 'NONE', *, *, #4000, .T. ) ;
#18601=EDGE_LOOP ( 'NONE', ( #14110, #3313, #21443, #9763 ) ) ;
#18612=DIRECTION ( 'NONE',  ( 7.125109674160325297E-05, -0.9999848031710253382, 0.005512562950849327591 ) ) ;
#18641=PLANE ( 'NONE',  #7087 ) ;
#18677=ORIENTED_EDGE ( 'NONE', *, *, #20455, .F. ) ;
#18695=DIRECTION ( 'NONE',  ( -0.01292394549866750231, -0.005513023399722823126, -0.9999012842304692006 ) ) ;
#18732=CARTESIAN_POINT ( 'NONE',  ( 19.43877198876942813, 177.6144908738019694, 111.1987526180507047 ) ) ;
#18736=AXIS2_PLACEMENT_3D ( 'NONE', #14095, #2234, #186 ) ;
#18764=CIRCLE ( 'NONE', #20954, 8.000000000000000000 ) ;
#18800=ORIENTED_EDGE ( 'NONE', *, *, #21724, .F. ) ;
#18856=ORIENTED_EDGE ( 'NONE', *, *, #8835, .F. ) ;
#18896=ORIENTED_EDGE ( 'NONE', *, *, #12164, .T. ) ;
#18900=DIRECTION ( 'NONE',  ( 7.125109674160325297E-05, -0.9999848031710252272, 0.005512562950849327591 ) ) ;
#18963=FACE_OUTER_BOUND ( 'NONE', #5, .T. ) ;
#19030=VERTEX_POINT ( 'NONE', #14366 ) ;
#19082=CARTESIAN_POINT ( 'NONE',  ( -11.19153202869804353, 137.5572120012638777, 101.3144779797563189 ) ) ;
#19104=CARTESIAN_POINT ( 'NONE',  ( 19.46476238196024866, 175.6255473142593360, 113.2095803124133511 ) ) ;
#19133=CARTESIAN_POINT ( 'NONE',  ( 13.76243855136152838, 137.5384677217048193, 97.59171006575670049 ) ) ;
#19139=DIRECTION ( 'NONE',  ( 7.125109674160325297E-05, -0.9999848031710252272, 0.005512562950849327591 ) ) ;
#19201=ORIENTED_EDGE ( 'NONE', *, *, #110, .F. ) ;
#19219=ORIENTED_EDGE ( 'NONE', *, *, #2949, .F. ) ;
#19222=FACE_OUTER_BOUND ( 'NONE', #20259, .T. ) ;
#19279=CARTESIAN_POINT ( 'NONE',  ( 19.43891449096291169, 175.6145212674599065, 111.2097777439524151 ) ) ;
#19336=ADVANCED_FACE ( 'NONE', ( #12608 ), #422, .F. ) ;
#19356=CARTESIAN_POINT ( 'NONE',  ( -14.53254043310009358, 177.6255169206013989, 113.6379760112694584 ) ) ;
#19369=LINE ( 'NONE', #3635, #9195 ) ;
#19404=DIRECTION ( 'NONE',  ( 7.125109674160325297E-05, -0.9999848031710252272, 0.005512562950849327591 ) ) ;
#19479=LINE ( 'NONE', #3751, #2733 ) ;
#19588=EDGE_LOOP ( 'NONE', ( #10811, #17781, #18262 ) ) ;
#19600=ORIENTED_EDGE ( 'NONE', *, *, #11113, .T. ) ;
#19620=ORIENTED_EDGE ( 'NONE', *, *, #11452, .F. ) ;
#19743=SURFACE_STYLE_FILL_AREA ( #17729 ) ;
#19751=CARTESIAN_POINT ( 'NONE',  ( -14.53254043310009358, 177.6255169206013989, 113.6379760112694584 ) ) ;
#19752=PLANE ( 'NONE',  #8218 ) ;
#19758=DIRECTION ( 'NONE',  ( -0.01292394549866737914, -0.005513023399720295634, -0.9999012842304692006 ) ) ;
#19763=FACE_OUTER_BOUND ( 'NONE', #8057, .T. ) ;
#19807=ORIENTED_EDGE ( 'NONE', *, *, #9478, .F. ) ;
#19871=DIRECTION ( 'NONE',  ( -0.01292394549866737914, -0.005513023399720295634, -0.9999012842304692006 ) ) ;
#19891=LINE ( 'NONE', #9692, #17198 ) ;
#19986=ORIENTED_EDGE ( 'NONE', *, *, #11600, .T. ) ;
#19989=DIRECTION ( 'NONE',  ( -0.01292394549866728373, -0.005513023399720296501, -0.9999012842304693116 ) ) ;
#19996=DIRECTION ( 'NONE',  ( 7.125109674160325297E-05, -0.9999848031710252272, 0.005512562950849327591 ) ) ;
#20063=ORIENTED_EDGE ( 'NONE', *, *, #8773, .T. ) ;
#20077=VERTEX_POINT ( 'NONE', #10485 ) ;
#20111=LINE ( 'NONE', #8062, #13169 ) ;
#20122=PLANE ( 'NONE',  #4038 ) ;
#20196=EDGE_CURVE ( 'NONE', #20403, #11929, #21401, .T. ) ;
#20219=CARTESIAN_POINT ( 'NONE',  ( -11.19153202869804353, 137.5572120012638777, 101.3144779797563189 ) ) ;
#20259=EDGE_LOOP ( 'NONE', ( #10242, #1596, #1369 ) ) ;
#20284=ORIENTED_EDGE ( 'NONE', *, *, #7520, .T. ) ;
#20296=CIRCLE ( 'NONE', #2710, 3.399999999999991918 ) ;
#20395=VERTEX_POINT ( 'NONE', #22555 ) ;
#20403=VERTEX_POINT ( 'NONE', #5114 ) ;
#20407=EDGE_LOOP ( 'NONE', ( #18856, #16788, #10266, #18440 ) ) ;
#20423=EDGE_CURVE ( 'NONE', #7668, #19030, #9881, .T. ) ;
#20455=EDGE_CURVE ( 'NONE', #20395, #17187, #20973, .T. ) ;
#20458=CARTESIAN_POINT ( 'NONE',  ( 1.143866695291850588, 165.4878681845327151, 88.49880848915942977 ) ) ;
#20499=DIRECTION ( 'NONE',  ( 0.01111468050521496539, -0.5103046645782702839, 0.8599218645824316942 ) ) ;
#20572=DIRECTION ( 'NONE',  ( 0.01292394549866728200, 0.005513023399720295634, 0.9999012842304692006 ) ) ;
#20670=ORIENTED_EDGE ( 'NONE', *, *, #20718, .T. ) ;
#20718=EDGE_CURVE ( 'NONE', #22024, #16835, #19479, .T. ) ;
#20740=EDGE_LOOP ( 'NONE', ( #19807, #21498, #337, #11771 ) ) ;
#20784=EDGE_LOOP ( 'NONE', ( #1412, #3746, #2277 ) ) ;
#20848=PLANE ( 'NONE',  #14837 ) ;
#20889=ORIENTED_EDGE ( 'NONE', *, *, #9478, .T. ) ;
#20890=ADVANCED_FACE ( 'NONE', ( #8228 ), #17301, .F. ) ;
#20954=AXIS2_PLACEMENT_3D ( 'NONE', #16153, #21392, #17876 ) ;
#20973=LINE ( 'NONE', #19133, #9707 ) ;
#21131=EDGE_LOOP ( 'NONE', ( #18591, #13918, #3988, #6044 ) ) ;
#21134=DIRECTION ( 'NONE',  ( -0.009088227368119913829, -0.7109943316365106014, -0.7031390079522376046 ) ) ;
#21187=CARTESIAN_POINT ( 'NONE',  ( 1.168872497073783157, 177.4987173824078468, 90.43346020349439129 ) ) ;
#21189=LINE ( 'NONE', #5443, #7629 ) ;
#21208=ORIENTED_EDGE ( 'NONE', *, *, #16113, .T. ) ;
#21227=ORIENTED_EDGE ( 'NONE', *, *, #11185, .F. ) ;
#21273=PRODUCT_DEFINITION_FORMATION_WITH_SPECIFIED_SOURCE ( 'ANY', '', #16046, .NOT_KNOWN. ) ;
#21309=DIRECTION ( 'NONE',  ( 0.6979091139780412290, -0.003898296230782321518, -0.7161757269782903501 ) ) ;
#21315=CARTESIAN_POINT ( 'NONE',  ( 19.43877198876942813, 177.6144908738019694, 111.1987526180507047 ) ) ;
#21361=ORIENTED_EDGE ( 'NONE', *, *, #4998, .F. ) ;
#21392=DIRECTION ( 'NONE',  ( 0.01292394549866728200, 0.005513023399720295634, 0.9999012842304692006 ) ) ;
#21401=CIRCLE ( 'NONE', #11523, 3.399999999999991918 ) ;
#21418=VECTOR ( 'NONE', #22568, 999.9999999999998863 ) ;
#21443=ORIENTED_EDGE ( 'NONE', *, *, #21724, .T. ) ;
#21449=CARTESIAN_POINT ( 'NONE',  ( 19.17021917716708046, 137.4993252555668164, 90.42132816724482325 ) ) ;
#21456=ORIENTED_EDGE ( 'NONE', *, *, #4275, .T. ) ;
#21473=ORIENTED_EDGE ( 'NONE', *, *, #1278, .F. ) ;
#21493=LINE ( 'NONE', #18294, #7997 ) ;
#21498=ORIENTED_EDGE ( 'NONE', *, *, #9253, .T. ) ;
#21574=EDGE_LOOP ( 'NONE', ( #21227, #7934 ) ) ;
#21604=EDGE_CURVE ( 'NONE', #11013, #5296, #5511, .T. ) ;
#21699=VERTEX_POINT ( 'NONE', #2429 ) ;
#21703=LINE ( 'NONE', #5990, #22609 ) ;
#21723=AXIS2_PLACEMENT_3D ( 'NONE', #897, #2725, #8115 ) ;
#21724=EDGE_CURVE ( 'NONE', #22024, #638, #4011, .T. ) ;
#21737=CARTESIAN_POINT ( 'NONE',  ( -11.23675596313486125, 155.5381941787832716, 97.81558748025744876 ) ) ;
#21865=FACE_OUTER_BOUND ( 'NONE', #18601, .T. ) ;
#22024=VERTEX_POINT ( 'NONE', #5255 ) ;
#22057=DIRECTION ( 'NONE',  ( 0.009188991635466195809, -0.7031977391749432149, 0.7109349492407668336 ) ) ;
#22140=VERTEX_POINT ( 'NONE', #12515 ) ;
#22245=EDGE_CURVE ( 'NONE', #20077, #15063, #16633, .T. ) ;
#22277=APPLICATION_CONTEXT ( 'automotive_design' ) ;
#22312=CARTESIAN_POINT ( 'NONE',  ( 13.80637996605699769, 137.5572120012638777, 100.9913744321402902 ) ) ;
#22336=FACE_OUTER_BOUND ( 'NONE', #19588, .T. ) ;
#22380=EDGE_CURVE ( 'NONE', #4461, #5296, #5641, .T. ) ;
#22410=SHAPE_REPRESENTATION_RELATIONSHIP ( 'NONE' , 'NONE' ,  #7092, #4147 ) ;
#22427=VECTOR ( 'NONE', #4130, 1000.000000000000114 ) ;
#22440=DIRECTION ( 'NONE',  ( -0.01292394549866750231, -0.005513023399722823126, -0.9999012842304692006 ) ) ;
#22472=CARTESIAN_POINT ( 'NONE',  ( -14.52969038923042966, 137.6261247937603969, 113.8584785293034400 ) ) ;
#22522=UNCERTAINTY_MEASURE_WITH_UNIT (LENGTH_MEASURE( 1.000000000000000082E-05 ), #5775, 'distance_accuracy_value', 'NONE');
#22523=EDGE_CURVE ( 'NONE', #16185, #11013, #6211, .T. ) ;
#22533=SURFACE_STYLE_USAGE ( .BOTH. , #8543 ) ;
#22555=CARTESIAN_POINT ( 'NONE',  ( 13.76115603162017820, 155.5381941787832716, 97.49248393264142010 ) ) ;
#22568=DIRECTION ( 'NONE',  ( -7.125109674160325297E-05, 0.9999848031710253382, -0.005512562950849327591 ) ) ;
#22580=DIRECTION ( 'NONE',  ( -0.7161863329816247070, -0.003898296230782349273, -0.6978982302147144212 ) ) ;
#22597=ORIENTED_EDGE ( 'NONE', *, *, #20196, .T. ) ;
#22609=VECTOR ( 'NONE', #19989, 999.9999999999998863 ) ;
ENDSEC;
END-ISO-10303-21;
